ISO-10303-21;
HEADER;
/* Generated by software containing ST-Developer
 * from STEP Tools, Inc. (www.steptools.com) 
 */

FILE_DESCRIPTION(
/* description */ ('Belt tension measurement rig'),
/* implementation_level */ '2;1');

FILE_NAME(
/* name */ 'Adjusting nut pedestal.step',
/* time_stamp */ '2026-10-28T03:24:44-07:00',
/* author */ (''),
/* organization */ (''),
/* preprocessor_version */ 'ST-DEVELOPER v20.2',
/* originating_system */ 'Autodesk Translation Framework v15.17.0.0',
/* authorisation */ '');

FILE_SCHEMA (('AUTOMOTIVE_DESIGN { 1 0 10303 214 3 1 1 }'));
ENDSEC;

DATA;
#10=MECHANICAL_DESIGN_GEOMETRIC_PRESENTATION_REPRESENTATION('',(#724),#23587);
#606=SHAPE_REPRESENTATION_RELATIONSHIP('SRR','None',#23853,#661);
#661=ADVANCED_BREP_SHAPE_REPRESENTATION('',(#794),#23551);
#724=STYLED_ITEM('',(#24218),#794);
#794=MANIFOLD_SOLID_BREP('Body1',#12229);
#962=FACE_BOUND('',#2497,.T.);
#963=FACE_BOUND('',#2500,.T.);
#964=FACE_BOUND('',#2503,.T.);
#965=FACE_BOUND('',#2504,.T.);
#1183=PLANE('',#13528);
#1184=PLANE('',#13532);
#1185=PLANE('',#13536);
#1186=PLANE('',#13537);
#1187=PLANE('',#13538);
#1188=PLANE('',#13539);
#1189=PLANE('',#13540);
#1190=PLANE('',#13541);
#1653=FACE_OUTER_BOUND('',#2490,.T.);
#1654=FACE_OUTER_BOUND('',#2491,.T.);
#1655=FACE_OUTER_BOUND('',#2492,.T.);
#1656=FACE_OUTER_BOUND('',#2493,.T.);
#1657=FACE_OUTER_BOUND('',#2494,.T.);
#1658=FACE_OUTER_BOUND('',#2495,.T.);
#1659=FACE_OUTER_BOUND('',#2496,.T.);
#1660=FACE_OUTER_BOUND('',#2498,.T.);
#1661=FACE_OUTER_BOUND('',#2499,.T.);
#1662=FACE_OUTER_BOUND('',#2501,.T.);
#1663=FACE_OUTER_BOUND('',#2502,.T.);
#2490=EDGE_LOOP('',(#9262,#9263,#9264,#9265));
#2491=EDGE_LOOP('',(#9266));
#2492=EDGE_LOOP('',(#9267,#9268,#9269,#9270));
#2493=EDGE_LOOP('',(#9271));
#2494=EDGE_LOOP('',(#9272,#9273,#9274,#9275));
#2495=EDGE_LOOP('',(#9276,#9277,#9278,#9279));
#2496=EDGE_LOOP('',(#9280,#9281,#9282,#9283));
#2497=EDGE_LOOP('',(#9284));
#2498=EDGE_LOOP('',(#9285,#9286,#9287,#9288));
#2499=EDGE_LOOP('',(#9289,#9290,#9291,#9292));
#2500=EDGE_LOOP('',(#9293));
#2501=EDGE_LOOP('',(#9294,#9295,#9296,#9297));
#2502=EDGE_LOOP('',(#9298,#9299,#9300,#9301));
#2503=EDGE_LOOP('',(#9302));
#2504=EDGE_LOOP('',(#9303));
#3294=LINE('',#20409,#4045);
#3295=LINE('',#20416,#4046);
#3296=LINE('',#20423,#4047);
#3297=LINE('',#20428,#4048);
#3298=LINE('',#20430,#4049);
#3299=LINE('',#20432,#4050);
#3300=LINE('',#20433,#4051);
#3301=LINE('',#20436,#4052);
#3302=LINE('',#20438,#4053);
#3303=LINE('',#20439,#4054);
#3304=LINE('',#20442,#4055);
#3305=LINE('',#20444,#4056);
#3306=LINE('',#20445,#4057);
#3307=LINE('',#20447,#4058);
#3308=LINE('',#20448,#4059);
#4045=VECTOR('',#16145,0.164999999999999);
#4046=VECTOR('',#16154,0.164999999999999);
#4047=VECTOR('',#16163,0.34);
#4048=VECTOR('',#16168,1.);
#4049=VECTOR('',#16169,1.);
#4050=VECTOR('',#16170,1.);
#4051=VECTOR('',#16171,1.);
#4052=VECTOR('',#16174,1.);
#4053=VECTOR('',#16175,1.);
#4054=VECTOR('',#16176,1.);
#4055=VECTOR('',#16179,1.);
#4056=VECTOR('',#16180,1.);
#4057=VECTOR('',#16181,1.);
#4058=VECTOR('',#16184,1.);
#4059=VECTOR('',#16185,1.);
#4784=CIRCLE('',#13526,0.164999999999999);
#4785=CIRCLE('',#13527,0.164999999999999);
#4786=CIRCLE('',#13530,0.164999999999999);
#4787=CIRCLE('',#13531,0.164999999999999);
#4788=CIRCLE('',#13534,0.34);
#4789=CIRCLE('',#13535,0.34);
#5686=VERTEX_POINT('',#20406);
#5687=VERTEX_POINT('',#20408);
#5688=VERTEX_POINT('',#20413);
#5689=VERTEX_POINT('',#20415);
#5690=VERTEX_POINT('',#20420);
#5691=VERTEX_POINT('',#20422);
#5692=VERTEX_POINT('',#20426);
#5693=VERTEX_POINT('',#20427);
#5694=VERTEX_POINT('',#20429);
#5695=VERTEX_POINT('',#20431);
#5696=VERTEX_POINT('',#20435);
#5697=VERTEX_POINT('',#20437);
#5698=VERTEX_POINT('',#20441);
#5699=VERTEX_POINT('',#20443);
#6990=EDGE_CURVE('',#5686,#5686,#4784,.T.);
#6991=EDGE_CURVE('',#5686,#5687,#3294,.T.);
#6992=EDGE_CURVE('',#5687,#5687,#4785,.T.);
#6993=EDGE_CURVE('',#5688,#5688,#4786,.T.);
#6994=EDGE_CURVE('',#5688,#5689,#3295,.T.);
#6995=EDGE_CURVE('',#5689,#5689,#4787,.T.);
#6996=EDGE_CURVE('',#5690,#5690,#4788,.T.);
#6997=EDGE_CURVE('',#5690,#5691,#3296,.T.);
#6998=EDGE_CURVE('',#5691,#5691,#4789,.T.);
#6999=EDGE_CURVE('',#5692,#5693,#3297,.T.);
#7000=EDGE_CURVE('',#5693,#5694,#3298,.T.);
#7001=EDGE_CURVE('',#5695,#5694,#3299,.T.);
#7002=EDGE_CURVE('',#5692,#5695,#3300,.T.);
#7003=EDGE_CURVE('',#5696,#5692,#3301,.T.);
#7004=EDGE_CURVE('',#5697,#5695,#3302,.T.);
#7005=EDGE_CURVE('',#5696,#5697,#3303,.T.);
#7006=EDGE_CURVE('',#5698,#5696,#3304,.T.);
#7007=EDGE_CURVE('',#5699,#5697,#3305,.T.);
#7008=EDGE_CURVE('',#5698,#5699,#3306,.T.);
#7009=EDGE_CURVE('',#5693,#5698,#3307,.T.);
#7010=EDGE_CURVE('',#5694,#5699,#3308,.T.);
#9262=ORIENTED_EDGE('',*,*,#6990,.F.);
#9263=ORIENTED_EDGE('',*,*,#6991,.T.);
#9264=ORIENTED_EDGE('',*,*,#6992,.T.);
#9265=ORIENTED_EDGE('',*,*,#6991,.F.);
#9266=ORIENTED_EDGE('',*,*,#6992,.F.);
#9267=ORIENTED_EDGE('',*,*,#6993,.F.);
#9268=ORIENTED_EDGE('',*,*,#6994,.T.);
#9269=ORIENTED_EDGE('',*,*,#6995,.T.);
#9270=ORIENTED_EDGE('',*,*,#6994,.F.);
#9271=ORIENTED_EDGE('',*,*,#6995,.F.);
#9272=ORIENTED_EDGE('',*,*,#6996,.F.);
#9273=ORIENTED_EDGE('',*,*,#6997,.T.);
#9274=ORIENTED_EDGE('',*,*,#6998,.F.);
#9275=ORIENTED_EDGE('',*,*,#6997,.F.);
#9276=ORIENTED_EDGE('',*,*,#6999,.T.);
#9277=ORIENTED_EDGE('',*,*,#7000,.T.);
#9278=ORIENTED_EDGE('',*,*,#7001,.F.);
#9279=ORIENTED_EDGE('',*,*,#7002,.F.);
#9280=ORIENTED_EDGE('',*,*,#7003,.T.);
#9281=ORIENTED_EDGE('',*,*,#7002,.T.);
#9282=ORIENTED_EDGE('',*,*,#7004,.F.);
#9283=ORIENTED_EDGE('',*,*,#7005,.F.);
#9284=ORIENTED_EDGE('',*,*,#6998,.T.);
#9285=ORIENTED_EDGE('',*,*,#7006,.T.);
#9286=ORIENTED_EDGE('',*,*,#7005,.T.);
#9287=ORIENTED_EDGE('',*,*,#7007,.F.);
#9288=ORIENTED_EDGE('',*,*,#7008,.F.);
#9289=ORIENTED_EDGE('',*,*,#7009,.T.);
#9290=ORIENTED_EDGE('',*,*,#7008,.T.);
#9291=ORIENTED_EDGE('',*,*,#7010,.F.);
#9292=ORIENTED_EDGE('',*,*,#7000,.F.);
#9293=ORIENTED_EDGE('',*,*,#6996,.T.);
#9294=ORIENTED_EDGE('',*,*,#7010,.T.);
#9295=ORIENTED_EDGE('',*,*,#7007,.T.);
#9296=ORIENTED_EDGE('',*,*,#7004,.T.);
#9297=ORIENTED_EDGE('',*,*,#7001,.T.);
#9298=ORIENTED_EDGE('',*,*,#7009,.F.);
#9299=ORIENTED_EDGE('',*,*,#6999,.F.);
#9300=ORIENTED_EDGE('',*,*,#7003,.F.);
#9301=ORIENTED_EDGE('',*,*,#7006,.F.);
#9302=ORIENTED_EDGE('',*,*,#6990,.T.);
#9303=ORIENTED_EDGE('',*,*,#6993,.T.);
#11291=CYLINDRICAL_SURFACE('',#13525,0.164999999999999);
#11292=CYLINDRICAL_SURFACE('',#13529,0.164999999999999);
#11293=CYLINDRICAL_SURFACE('',#13533,0.34);
#11794=ADVANCED_FACE('',(#1653),#11291,.F.);
#11795=ADVANCED_FACE('',(#1654),#1183,.F.);
#11796=ADVANCED_FACE('',(#1655),#11292,.F.);
#11797=ADVANCED_FACE('',(#1656),#1184,.F.);
#11798=ADVANCED_FACE('',(#1657),#11293,.F.);
#11799=ADVANCED_FACE('',(#1658),#1185,.T.);
#11800=ADVANCED_FACE('',(#1659,#962),#1186,.T.);
#11801=ADVANCED_FACE('',(#1660),#1187,.T.);
#11802=ADVANCED_FACE('',(#1661,#963),#1188,.T.);
#11803=ADVANCED_FACE('',(#1662),#1189,.T.);
#11804=ADVANCED_FACE('',(#1663,#964,#965),#1190,.F.);
#12229=CLOSED_SHELL('',(#11794,#11795,#11796,#11797,#11798,#11799,#11800,
#11801,#11802,#11803,#11804));
#13524=AXIS2_PLACEMENT_3D('',#20404,#16139,#16140);
#13525=AXIS2_PLACEMENT_3D('',#20405,#16141,#16142);
#13526=AXIS2_PLACEMENT_3D('',#20407,#16143,#16144);
#13527=AXIS2_PLACEMENT_3D('',#20410,#16146,#16147);
#13528=AXIS2_PLACEMENT_3D('',#20411,#16148,#16149);
#13529=AXIS2_PLACEMENT_3D('',#20412,#16150,#16151);
#13530=AXIS2_PLACEMENT_3D('',#20414,#16152,#16153);
#13531=AXIS2_PLACEMENT_3D('',#20417,#16155,#16156);
#13532=AXIS2_PLACEMENT_3D('',#20418,#16157,#16158);
#13533=AXIS2_PLACEMENT_3D('',#20419,#16159,#16160);
#13534=AXIS2_PLACEMENT_3D('',#20421,#16161,#16162);
#13535=AXIS2_PLACEMENT_3D('',#20424,#16164,#16165);
#13536=AXIS2_PLACEMENT_3D('',#20425,#16166,#16167);
#13537=AXIS2_PLACEMENT_3D('',#20434,#16172,#16173);
#13538=AXIS2_PLACEMENT_3D('',#20440,#16177,#16178);
#13539=AXIS2_PLACEMENT_3D('',#20446,#16182,#16183);
#13540=AXIS2_PLACEMENT_3D('',#20449,#16186,#16187);
#13541=AXIS2_PLACEMENT_3D('',#20450,#16188,#16189);
#16139=DIRECTION('axis',(0.,0.,1.));
#16140=DIRECTION('refdir',(1.,0.,0.));
#16141=DIRECTION('center_axis',(0.,0.,1.));
#16142=DIRECTION('ref_axis',(1.,0.,0.));
#16143=DIRECTION('center_axis',(0.,0.,1.));
#16144=DIRECTION('ref_axis',(1.,0.,0.));
#16145=DIRECTION('',(0.,0.,1.));
#16146=DIRECTION('center_axis',(0.,0.,1.));
#16147=DIRECTION('ref_axis',(1.,0.,0.));
#16148=DIRECTION('center_axis',(0.,0.,1.));
#16149=DIRECTION('ref_axis',(1.,0.,0.));
#16150=DIRECTION('center_axis',(0.,0.,1.));
#16151=DIRECTION('ref_axis',(1.,0.,0.));
#16152=DIRECTION('center_axis',(0.,0.,1.));
#16153=DIRECTION('ref_axis',(1.,0.,0.));
#16154=DIRECTION('',(0.,0.,1.));
#16155=DIRECTION('center_axis',(0.,0.,1.));
#16156=DIRECTION('ref_axis',(1.,0.,0.));
#16157=DIRECTION('center_axis',(0.,0.,1.));
#16158=DIRECTION('ref_axis',(1.,0.,0.));
#16159=DIRECTION('center_axis',(1.,0.,0.));
#16160=DIRECTION('ref_axis',(0.,0.,-1.));
#16161=DIRECTION('center_axis',(1.,0.,0.));
#16162=DIRECTION('ref_axis',(0.,0.,-1.));
#16163=DIRECTION('',(1.,0.,0.));
#16164=DIRECTION('center_axis',(-1.,0.,0.));
#16165=DIRECTION('ref_axis',(0.,0.,-1.));
#16166=DIRECTION('center_axis',(0.,1.,0.));
#16167=DIRECTION('ref_axis',(-1.,0.,0.));
#16168=DIRECTION('',(-1.,0.,0.));
#16169=DIRECTION('',(0.,0.,1.));
#16170=DIRECTION('',(-1.,0.,0.));
#16171=DIRECTION('',(0.,0.,1.));
#16172=DIRECTION('center_axis',(1.,0.,0.));
#16173=DIRECTION('ref_axis',(0.,1.,0.));
#16174=DIRECTION('',(0.,1.,0.));
#16175=DIRECTION('',(0.,1.,0.));
#16176=DIRECTION('',(0.,0.,1.));
#16177=DIRECTION('center_axis',(0.,-1.,0.));
#16178=DIRECTION('ref_axis',(1.,0.,0.));
#16179=DIRECTION('',(1.,0.,0.));
#16180=DIRECTION('',(1.,0.,0.));
#16181=DIRECTION('',(0.,0.,1.));
#16182=DIRECTION('center_axis',(-1.,0.,0.));
#16183=DIRECTION('ref_axis',(0.,-1.,0.));
#16184=DIRECTION('',(0.,-1.,0.));
#16185=DIRECTION('',(0.,-1.,0.));
#16186=DIRECTION('center_axis',(0.,0.,1.));
#16187=DIRECTION('ref_axis',(1.,0.,0.));
#16188=DIRECTION('center_axis',(0.,0.,1.));
#16189=DIRECTION('ref_axis',(1.,0.,0.));
#20404=CARTESIAN_POINT('',(0.,0.,0.));
#20405=CARTESIAN_POINT('Origin',(12.5,11.7,3.1));
#20406=CARTESIAN_POINT('',(12.335,11.7,3.2));
#20407=CARTESIAN_POINT('Origin',(12.5,11.7,3.2));
#20408=CARTESIAN_POINT('',(12.335,11.7,4.1));
#20409=CARTESIAN_POINT('',(12.335,11.7,3.1));
#20410=CARTESIAN_POINT('Origin',(12.5,11.7,4.1));
#20411=CARTESIAN_POINT('Origin',(12.5,11.7,4.1));
#20412=CARTESIAN_POINT('Origin',(11.5,10.3,3.1));
#20413=CARTESIAN_POINT('',(11.335,10.3,3.2));
#20414=CARTESIAN_POINT('Origin',(11.5,10.3,3.2));
#20415=CARTESIAN_POINT('',(11.335,10.3,4.1));
#20416=CARTESIAN_POINT('',(11.335,10.3,3.1));
#20417=CARTESIAN_POINT('Origin',(11.5,10.3,4.1));
#20418=CARTESIAN_POINT('Origin',(11.5,10.3,4.1));
#20419=CARTESIAN_POINT('Origin',(10.9,11.,4.5));
#20420=CARTESIAN_POINT('',(11.,11.,4.84));
#20421=CARTESIAN_POINT('Origin',(11.,11.,4.5));
#20422=CARTESIAN_POINT('',(13.,11.,4.84));
#20423=CARTESIAN_POINT('',(10.9,11.,4.84));
#20424=CARTESIAN_POINT('Origin',(13.,11.,4.5));
#20425=CARTESIAN_POINT('Origin',(13.,12.,3.2));
#20426=CARTESIAN_POINT('',(13.,12.,3.2));
#20427=CARTESIAN_POINT('',(11.,12.,3.2));
#20428=CARTESIAN_POINT('',(13.,12.,3.2));
#20429=CARTESIAN_POINT('',(11.,12.,5.7));
#20430=CARTESIAN_POINT('',(11.,12.,3.2));
#20431=CARTESIAN_POINT('',(13.,12.,5.7));
#20432=CARTESIAN_POINT('',(13.,12.,5.7));
#20433=CARTESIAN_POINT('',(13.,12.,3.2));
#20434=CARTESIAN_POINT('Origin',(13.,10.,3.2));
#20435=CARTESIAN_POINT('',(13.,10.,3.2));
#20436=CARTESIAN_POINT('',(13.,10.,3.2));
#20437=CARTESIAN_POINT('',(13.,10.,5.7));
#20438=CARTESIAN_POINT('',(13.,10.,5.7));
#20439=CARTESIAN_POINT('',(13.,10.,3.2));
#20440=CARTESIAN_POINT('Origin',(11.,10.,3.2));
#20441=CARTESIAN_POINT('',(11.,10.,3.2));
#20442=CARTESIAN_POINT('',(11.,10.,3.2));
#20443=CARTESIAN_POINT('',(11.,10.,5.7));
#20444=CARTESIAN_POINT('',(11.,10.,5.7));
#20445=CARTESIAN_POINT('',(11.,10.,3.2));
#20446=CARTESIAN_POINT('Origin',(11.,12.,3.2));
#20447=CARTESIAN_POINT('',(11.,12.,3.2));
#20448=CARTESIAN_POINT('',(11.,12.,5.7));
#20449=CARTESIAN_POINT('Origin',(12.,11.,5.7));
#20450=CARTESIAN_POINT('Origin',(12.,11.,3.2));
#23486=UNCERTAINTY_MEASURE_WITH_UNIT(LENGTH_MEASURE(0.001),#23588,
'DISTANCE_ACCURACY_VALUE',
'Maximum model space distance between geometric entities at asserted c
onnectivities');
#23522=UNCERTAINTY_MEASURE_WITH_UNIT(LENGTH_MEASURE(0.001),#23588,
'DISTANCE_ACCURACY_VALUE',
'Maximum model space distance between geometric entities at asserted c
onnectivities');
#23551=(
GEOMETRIC_REPRESENTATION_CONTEXT(3)
GLOBAL_UNCERTAINTY_ASSIGNED_CONTEXT((#23486))
GLOBAL_UNIT_ASSIGNED_CONTEXT((#23588,#23590,#23591))
REPRESENTATION_CONTEXT('','3D')
);
#23587=(
GEOMETRIC_REPRESENTATION_CONTEXT(3)
GLOBAL_UNCERTAINTY_ASSIGNED_CONTEXT((#23522))
GLOBAL_UNIT_ASSIGNED_CONTEXT((#23588,#23590,#23591))
REPRESENTATION_CONTEXT('','3D')
);
#23588=(
LENGTH_UNIT()
NAMED_UNIT(*)
SI_UNIT(.CENTI.,.METRE.)
);
#23590=(
NAMED_UNIT(*)
PLANE_ANGLE_UNIT()
SI_UNIT($,.RADIAN.)
);
#23591=(
NAMED_UNIT(*)
SI_UNIT($,.STERADIAN.)
SOLID_ANGLE_UNIT()
);
#23620=SHAPE_DEFINITION_REPRESENTATION(#23689,#23853);
#23689=PRODUCT_DEFINITION_SHAPE('',$,#23918);
#23853=SHAPE_REPRESENTATION('',(#13524),#23551);
#23889=PRODUCT_DEFINITION_CONTEXT('part definition',#24083,'design');
#23918=PRODUCT_DEFINITION('Adjusting nut pedestal',
'Adjusting nut pedestal',#23982,#23889);
#23982=PRODUCT_DEFINITION_FORMATION('',$,#24113);
#24083=APPLICATION_CONTEXT(
'Core Data for Automotive Mechanical Design Process');
#24084=PRODUCT_CONTEXT('part definition',#24083,'mechanical');
#24113=PRODUCT('Adjusting nut pedestal','Adjusting nut pedestal',
'Adjusting nut pedestal',(#24084));
#24212=COLOUR_RGB('Black',0.12,0.14,0.17);
#24213=FILL_AREA_STYLE_COLOUR('',#24212);
#24214=FILL_AREA_STYLE('',(#24213));
#24215=SURFACE_STYLE_FILL_AREA(#24214);
#24216=SURFACE_SIDE_STYLE('',(#24215));
#24217=SURFACE_STYLE_USAGE(.BOTH.,#24216);
#24218=PRESENTATION_STYLE_ASSIGNMENT((#24217));
ENDSEC;
END-ISO-10303-21;
